ISO-10303-21;
HEADER;
FILE_DESCRIPTION (('STEP AP214'),
    '1' );
FILE_NAME ('plain washer 10669 type nl_iso_ISO 10669-5.4-N.step',
    '2026-10-24T08:20:21',
    ( '' ),
    ( '' ),
    'SwSTEP 2.0',
    'SolidWorks 2026',
    '' );
FILE_SCHEMA (( 'AUTOMOTIVE_DESIGN' ));
ENDSEC;

DATA;
#16=CARTESIAN_POINT ( 'NONE',  ( 0.000000000000000000, 8.572527594031473190E-16, -7.000000000000000000 ) ) ;
#95=CARTESIAN_POINT ( 'NONE',  ( 1.600000000000000089, 0.000000000000000000, 0.000000000000000000 ) ) ;
#123=EDGE_LOOP ( 'NONE', ( #2898, #2234 ) ) ;
#144=DIRECTION ( 'NONE',  ( 1.000000000000000000, 0.000000000000000000, 0.000000000000000000 ) ) ;
#147=DIRECTION ( 'NONE',  ( -1.000000000000000000, -0.000000000000000000, -0.000000000000000000 ) ) ;
#158=VECTOR ( 'NONE', #3390, 1000.000000000000000 ) ;
#163=DIRECTION ( 'NONE',  ( 0.000000000000000000, 0.000000000000000000, -1.000000000000000000 ) ) ;
#168=DIRECTION ( 'NONE',  ( 0.000000000000000000, 0.000000000000000000, -1.000000000000000000 ) ) ;
#185=CARTESIAN_POINT ( 'NONE',  ( 0.000000000000000000, 0.000000000000000000, 0.000000000000000000 ) ) ;
#201=VERTEX_POINT ( 'NONE', #243 ) ;
#205=CYLINDRICAL_SURFACE ( 'NONE', #444, 2.700000000000000178 ) ;
#208=VERTEX_POINT ( 'NONE', #3226 ) ;
#225=DIRECTION ( 'NONE',  ( -1.000000000000000000, -0.000000000000000000, -0.000000000000000000 ) ) ;
#243=CARTESIAN_POINT ( 'NONE',  ( 0.000000000000000000, 0.000000000000000000, 7.000000000000000000 ) ) ;
#247=FACE_BOUND ( 'NONE', #351, .T. ) ;
#264=ORIENTED_EDGE ( 'NONE', *, *, #1371, .T. ) ;
#277=CARTESIAN_POINT ( 'NONE',  ( 1.600000000000000089, 0.000000000000000000, 2.700000000000000178 ) ) ;
#291=DIRECTION ( 'NONE',  ( 1.000000000000000000, 0.000000000000000000, 0.000000000000000000 ) ) ;
#351=EDGE_LOOP ( 'NONE', ( #1007, #874 ) ) ;
#376=( NAMED_UNIT ( * ) SI_UNIT ( $, .STERADIAN. ) SOLID_ANGLE_UNIT ( ) );
#420=CARTESIAN_POINT ( 'NONE',  ( 1.600000000000000089, 8.572527594031473190E-16, -7.000000000000000000 ) ) ;
#444=AXIS2_PLACEMENT_3D ( 'NONE', #1397, #2583, #1222 ) ;
#469=AXIS2_PLACEMENT_3D ( 'NONE', #940, #1573, #3367 ) ;
#525=DIRECTION ( 'NONE',  ( 0.000000000000000000, 0.000000000000000000, -1.000000000000000000 ) ) ;
#538=DIRECTION ( 'NONE',  ( 0.000000000000000000, 0.000000000000000000, 1.000000000000000000 ) ) ;
#547=CARTESIAN_POINT ( 'NONE',  ( 0.000000000000000000, 0.000000000000000000, 0.000000000000000000 ) ) ;
#601=ORIENTED_EDGE ( 'NONE', *, *, #3693, .F. ) ;
#640=AXIS2_PLACEMENT_3D ( 'NONE', #2895, #225, #538 ) ;
#669=ORIENTED_EDGE ( 'NONE', *, *, #2050, .F. ) ;
#693=MANIFOLD_SOLID_BREP ( 'Base-Extrude', #871 ) ;
#695=LINE ( 'NONE', #2173, #833 ) ;
#713=DIRECTION ( 'NONE',  ( 1.000000000000000000, 0.000000000000000000, 0.000000000000000000 ) ) ;
#714=DIRECTION ( 'NONE',  ( -1.000000000000000000, -0.000000000000000000, -0.000000000000000000 ) ) ;
#725=SURFACE_STYLE_USAGE ( .BOTH. , #997 ) ;
#739=DIRECTION ( 'NONE',  ( -1.000000000000000000, -0.000000000000000000, -0.000000000000000000 ) ) ;
#741=( LENGTH_UNIT ( ) NAMED_UNIT ( * ) SI_UNIT ( .MILLI., .METRE. ) );
#748=VERTEX_POINT ( 'NONE', #1266 ) ;
#786=CIRCLE ( 'NONE', #469, 7.000000000000000000 ) ;
#801=CARTESIAN_POINT ( 'NONE',  ( 1.600000000000000089, 0.000000000000000000, 0.000000000000000000 ) ) ;
#811=CARTESIAN_POINT ( 'NONE',  ( 1.600000000000000089, 0.000000000000000000, 2.700000000000000178 ) ) ;
#820=CARTESIAN_POINT ( 'NONE',  ( 0.000000000000000000, 0.000000000000000000, 0.000000000000000000 ) ) ;
#833=VECTOR ( 'NONE', #739, 1000.000000000000000 ) ;
#834=FACE_OUTER_BOUND ( 'NONE', #3097, .T. ) ;
#855=EDGE_CURVE ( 'NONE', #1639, #1544, #2142, .T. ) ;
#871=CLOSED_SHELL ( 'NONE', ( #2181, #2910, #1552, #3450, #2335, #2348 ) ) ;
#874=ORIENTED_EDGE ( 'NONE', *, *, #3658, .F. ) ;
#940=CARTESIAN_POINT ( 'NONE',  ( 1.600000000000000089, 0.000000000000000000, 0.000000000000000000 ) ) ;
#997=SURFACE_SIDE_STYLE ('',( #2471 ) ) ;
#1007=ORIENTED_EDGE ( 'NONE', *, *, #3276, .F. ) ;
#1036=( NAMED_UNIT ( * ) SI_UNIT ( $, .STERADIAN. ) SOLID_ANGLE_UNIT ( ) );
#1049=ORIENTED_EDGE ( 'NONE', *, *, #3120, .F. ) ;
#1053=CARTESIAN_POINT ( 'NONE',  ( 1.600000000000000089, 0.000000000000000000, 0.000000000000000000 ) ) ;
#1098=MECHANICAL_DESIGN_GEOMETRIC_PRESENTATION_REPRESENTATION('',(#3026),#1155);
#1118=EDGE_LOOP ( 'NONE', ( #1839, #264, #1666, #669 ) ) ;
#1123=ORIENTED_EDGE ( 'NONE', *, *, #2637, .T. ) ;
#1145=AXIS2_PLACEMENT_3D ( 'NONE', #95, #2202, #2745 ) ;
#1155=( GEOMETRIC_REPRESENTATION_CONTEXT ( 3 ) GLOBAL_UNCERTAINTY_ASSIGNED_CONTEXT ( ( #1207 ) ) GLOBAL_UNIT_ASSIGNED_CONTEXT ( ( #741, #1628, #1036 ) ) REPRESENTATION_CONTEXT ( 'NONE', 'WORKASPACE' ) );
#1175=APPLICATION_CONTEXT ( 'automotive_design' ) ;
#1182=EDGE_LOOP ( 'NONE', ( #3240, #3707, #2855, #1049 ) ) ;
#1198=CIRCLE ( 'NONE', #3185, 7.000000000000000000 ) ;
#1207=UNCERTAINTY_MEASURE_WITH_UNIT (LENGTH_MEASURE( 1.000000000000000082E-05 ), #741, 'distance_accuracy_value', 'NONE');
#1222=DIRECTION ( 'NONE',  ( 0.000000000000000000, 0.000000000000000000, 1.000000000000000000 ) ) ;
#1232=PRODUCT_DEFINITION ( 'UNKNOWN', '', #3270, #1246 ) ;
#1245=EDGE_CURVE ( 'NONE', #3752, #748, #786, .T. ) ;
#1246=PRODUCT_DEFINITION_CONTEXT ( 'detailed design', #1566, 'design' ) ;
#1253=EDGE_LOOP ( 'NONE', ( #3192, #1444 ) ) ;
#1266=CARTESIAN_POINT ( 'NONE',  ( 1.600000000000000089, 8.572527594031473190E-16, -7.000000000000000000 ) ) ;
#1281=VERTEX_POINT ( 'NONE', #277 ) ;
#1293=ORIENTED_EDGE ( 'NONE', *, *, #2111, .F. ) ;
#1306=CARTESIAN_POINT ( 'NONE',  ( 0.000000000000000000, 0.000000000000000000, 0.000000000000000000 ) ) ;
#1334=CARTESIAN_POINT ( 'NONE',  ( 0.000000000000000000, 0.000000000000000000, 0.000000000000000000 ) ) ;
#1355=FACE_OUTER_BOUND ( 'NONE', #1118, .T. ) ;
#1371=EDGE_CURVE ( 'NONE', #748, #2736, #1973, .T. ) ;
#1389=CIRCLE ( 'NONE', #2195, 2.700000000000000178 ) ;
#1397=CARTESIAN_POINT ( 'NONE',  ( 1.600000000000000089, 0.000000000000000000, 0.000000000000000000 ) ) ;
#1434=PLANE ( 'NONE',  #2376 ) ;
#1440=CIRCLE ( 'NONE', #2569, 2.700000000000000178 ) ;
#1444=ORIENTED_EDGE ( 'NONE', *, *, #2111, .T. ) ;
#1459=MECHANICAL_DESIGN_GEOMETRIC_PRESENTATION_REPRESENTATION('',(#2338),#1836);
#1461=DIRECTION ( 'NONE',  ( 0.000000000000000000, 0.000000000000000000, -1.000000000000000000 ) ) ;
#1472=DIRECTION ( 'NONE',  ( 0.000000000000000000, 0.000000000000000000, -1.000000000000000000 ) ) ;
#1499=ORIENTED_EDGE ( 'NONE', *, *, #1245, .F. ) ;
#1518=AXIS2_PLACEMENT_3D ( 'NONE', #1334, #144, #168 ) ;
#1543=DIRECTION ( 'NONE',  ( 1.000000000000000000, 0.000000000000000000, 0.000000000000000000 ) ) ;
#1544=VERTEX_POINT ( 'NONE', #1774 ) ;
#1552=ADVANCED_FACE ( 'NONE', ( #1749, #247 ), #1434, .T. ) ;
#1566=APPLICATION_CONTEXT ( 'automotive_design' ) ;
#1573=DIRECTION ( 'NONE',  ( 1.000000000000000000, 0.000000000000000000, 0.000000000000000000 ) ) ;
#1609=SHAPE_REPRESENTATION_RELATIONSHIP ( 'NONE' , 'NONE' ,  #2949, #2598 ) ;
#1628=( NAMED_UNIT ( * ) PLANE_ANGLE_UNIT ( ) SI_UNIT ( $, .RADIAN. ) );
#1639=VERTEX_POINT ( 'NONE', #1831 ) ;
#1659=PRODUCT_CONTEXT ( 'NONE', #1175, 'mechanical' ) ;
#1666=ORIENTED_EDGE ( 'NONE', *, *, #3693, .T. ) ;
#1678=SHAPE_DEFINITION_REPRESENTATION ( #3337, #2949 ) ;
#1749=FACE_OUTER_BOUND ( 'NONE', #123, .T. ) ;
#1774=CARTESIAN_POINT ( 'NONE',  ( 0.000000000000000000, 3.306546357697853733E-16, -2.700000000000000178 ) ) ;
#1822=AXIS2_PLACEMENT_3D ( 'NONE', #1306, #3627, #3351 ) ;
#1831=CARTESIAN_POINT ( 'NONE',  ( 0.000000000000000000, 0.000000000000000000, 2.700000000000000178 ) ) ;
#1836=( GEOMETRIC_REPRESENTATION_CONTEXT ( 3 ) GLOBAL_UNCERTAINTY_ASSIGNED_CONTEXT ( ( #3509 ) ) GLOBAL_UNIT_ASSIGNED_CONTEXT ( ( #3759, #2289, #2508 ) ) REPRESENTATION_CONTEXT ( 'NONE', 'WORKASPACE' ) );
#1839=ORIENTED_EDGE ( 'NONE', *, *, #1896, .F. ) ;
#1854=ORIENTED_EDGE ( 'NONE', *, *, #2283, .F. ) ;
#1862=FILL_AREA_STYLE ('',( #3657 ) ) ;
#1896=EDGE_CURVE ( 'NONE', #748, #3752, #1198, .T. ) ;
#1898=( GEOMETRIC_REPRESENTATION_CONTEXT ( 3 ) GLOBAL_UNCERTAINTY_ASSIGNED_CONTEXT ( ( #1996 ) ) GLOBAL_UNIT_ASSIGNED_CONTEXT ( ( #2450, #2177, #376 ) ) REPRESENTATION_CONTEXT ( 'NONE', 'WORKASPACE' ) );
#1917=DIRECTION ( 'NONE',  ( 0.000000000000000000, 0.000000000000000000, 1.000000000000000000 ) ) ;
#1941=ORIENTED_EDGE ( 'NONE', *, *, #2637, .F. ) ;
#1973=LINE ( 'NONE', #420, #158 ) ;
#1996=UNCERTAINTY_MEASURE_WITH_UNIT (LENGTH_MEASURE( 1.000000000000000082E-05 ), #2450, 'distance_accuracy_value', 'NONE');
#2000=DIRECTION ( 'NONE',  ( -1.000000000000000000, -0.000000000000000000, -0.000000000000000000 ) ) ;
#2006=CARTESIAN_POINT ( 'NONE',  ( 1.600000000000000089, 0.000000000000000000, 0.000000000000000000 ) ) ;
#2039=DIRECTION ( 'NONE',  ( -1.000000000000000000, -0.000000000000000000, -0.000000000000000000 ) ) ;
#2050=EDGE_CURVE ( 'NONE', #3752, #201, #695, .T. ) ;
#2107=FACE_BOUND ( 'NONE', #1253, .T. ) ;
#2111=EDGE_CURVE ( 'NONE', #1544, #1639, #1389, .T. ) ;
#2142=CIRCLE ( 'NONE', #1518, 2.700000000000000178 ) ;
#2145=COLOUR_RGB ( '',1.000000000000000000, 0.9490196078431372140, 0.9098039215686274384 ) ;
#2173=CARTESIAN_POINT ( 'NONE',  ( 1.600000000000000089, 0.000000000000000000, 7.000000000000000000 ) ) ;
#2177=( NAMED_UNIT ( * ) PLANE_ANGLE_UNIT ( ) SI_UNIT ( $, .RADIAN. ) );
#2180=CARTESIAN_POINT ( 'NONE',  ( 1.600000000000000089, 0.000000000000000000, 7.000000000000000000 ) ) ;
#2181=ADVANCED_FACE ( 'NONE', ( #2530 ), #2839, .F. ) ;
#2195=AXIS2_PLACEMENT_3D ( 'NONE', #185, #3421, #3669 ) ;
#2202=DIRECTION ( 'NONE',  ( 1.000000000000000000, 0.000000000000000000, 0.000000000000000000 ) ) ;
#2207=AXIS2_PLACEMENT_3D ( 'NONE', #820, #2246, #3194 ) ;
#2234=ORIENTED_EDGE ( 'NONE', *, *, #1896, .T. ) ;
#2246=DIRECTION ( 'NONE',  ( 0.000000000000000000, 0.000000000000000000, 1.000000000000000000 ) ) ;
#2262=PRESENTATION_STYLE_ASSIGNMENT (( #725 ) ) ;
#2283=EDGE_CURVE ( 'NONE', #208, #1544, #3791, .T. ) ;
#2289=( NAMED_UNIT ( * ) PLANE_ANGLE_UNIT ( ) SI_UNIT ( $, .RADIAN. ) );
#2290=FACE_OUTER_BOUND ( 'NONE', #3628, .T. ) ;
#2327=CIRCLE ( 'NONE', #1145, 2.700000000000000178 ) ;
#2334=CARTESIAN_POINT ( 'NONE',  ( 1.600000000000000089, 3.306546357697853733E-16, -2.700000000000000178 ) ) ;
#2335=ADVANCED_FACE ( 'NONE', ( #834 ), #3207, .T. ) ;
#2338=STYLED_ITEM ( 'NONE', ( #2262 ), #2598 ) ;
#2348=ADVANCED_FACE ( 'NONE', ( #2933 ), #205, .F. ) ;
#2376=AXIS2_PLACEMENT_3D ( 'NONE', #2006, #291, #525 ) ;
#2450=( LENGTH_UNIT ( ) NAMED_UNIT ( * ) SI_UNIT ( .MILLI., .METRE. ) );
#2471=SURFACE_STYLE_FILL_AREA ( #1862 ) ;
#2500=AXIS2_PLACEMENT_3D ( 'NONE', #547, #2675, #1461 ) ;
#2508=( NAMED_UNIT ( * ) SI_UNIT ( $, .STERADIAN. ) SOLID_ANGLE_UNIT ( ) );
#2530=FACE_OUTER_BOUND ( 'NONE', #1182, .T. ) ;
#2569=AXIS2_PLACEMENT_3D ( 'NONE', #3125, #1543, #2806 ) ;
#2583=DIRECTION ( 'NONE',  ( -1.000000000000000000, -0.000000000000000000, -0.000000000000000000 ) ) ;
#2598=ADVANCED_BREP_SHAPE_REPRESENTATION ( '', ( #693, #2207 ), #1898 ) ;
#2637=EDGE_CURVE ( 'NONE', #201, #2736, #3378, .T. ) ;
#2675=DIRECTION ( 'NONE',  ( 1.000000000000000000, 0.000000000000000000, 0.000000000000000000 ) ) ;
#2695=VECTOR ( 'NONE', #2000, 1000.000000000000000 ) ;
#2736=VERTEX_POINT ( 'NONE', #16 ) ;
#2745=DIRECTION ( 'NONE',  ( 0.000000000000000000, 0.000000000000000000, -1.000000000000000000 ) ) ;
#2806=DIRECTION ( 'NONE',  ( 0.000000000000000000, 0.000000000000000000, -1.000000000000000000 ) ) ;
#2815=AXIS2_PLACEMENT_3D ( 'NONE', #2816, #147, #3716 ) ;
#2816=CARTESIAN_POINT ( 'NONE',  ( 1.600000000000000089, 0.000000000000000000, 0.000000000000000000 ) ) ;
#2831=CARTESIAN_POINT ( 'NONE',  ( 0.000000000000000000, 0.000000000000000000, 0.000000000000000000 ) ) ;
#2839=CYLINDRICAL_SURFACE ( 'NONE', #2815, 2.700000000000000178 ) ;
#2855=ORIENTED_EDGE ( 'NONE', *, *, #855, .F. ) ;
#2874=VECTOR ( 'NONE', #2039, 1000.000000000000000 ) ;
#2895=CARTESIAN_POINT ( 'NONE',  ( 1.600000000000000089, 0.000000000000000000, 0.000000000000000000 ) ) ;
#2898=ORIENTED_EDGE ( 'NONE', *, *, #1245, .T. ) ;
#2910=ADVANCED_FACE ( 'NONE', ( #1355 ), #3688, .T. ) ;
#2933=FACE_OUTER_BOUND ( 'NONE', #3411, .T. ) ;
#2949=SHAPE_REPRESENTATION ( 'plain washer 10669 type nl_iso_ISO 10669-5.4-N', ( #2207 ), #1898 ) ;
#3026=STYLED_ITEM('',(#3881),#693);
#3055=ORIENTED_EDGE ( 'NONE', *, *, #3120, .T. ) ;
#3078=AXIS2_PLACEMENT_3D ( 'NONE', #1053, #714, #1917 ) ;
#3097=EDGE_LOOP ( 'NONE', ( #3187, #1499, #3485, #1123 ) ) ;
#3110=ORIENTED_EDGE ( 'NONE', *, *, #3658, .T. ) ;
#3120=EDGE_CURVE ( 'NONE', #1281, #1639, #3511, .T. ) ;
#3125=CARTESIAN_POINT ( 'NONE',  ( 1.600000000000000089, 0.000000000000000000, 0.000000000000000000 ) ) ;
#3185=AXIS2_PLACEMENT_3D ( 'NONE', #801, #3537, #1472 ) ;
#3187=ORIENTED_EDGE ( 'NONE', *, *, #1371, .F. ) ;
#3192=ORIENTED_EDGE ( 'NONE', *, *, #855, .T. ) ;
#3194=DIRECTION ( 'NONE',  ( 1.000000000000000000, 0.000000000000000000, 0.000000000000000000 ) ) ;
#3207=CYLINDRICAL_SURFACE ( 'NONE', #640, 7.000000000000000000 ) ;
#3226=CARTESIAN_POINT ( 'NONE',  ( 1.600000000000000089, 3.306546357697853733E-16, -2.700000000000000178 ) ) ;
#3240=ORIENTED_EDGE ( 'NONE', *, *, #3276, .T. ) ;
#3270=PRODUCT_DEFINITION_FORMATION_WITH_SPECIFIED_SOURCE ( 'ANY', '', #3612, .NOT_KNOWN. ) ;
#3276=EDGE_CURVE ( 'NONE', #1281, #208, #1440, .T. ) ;
#3291=PLANE ( 'NONE',  #2500 ) ;
#3337=PRODUCT_DEFINITION_SHAPE ( 'NONE', 'NONE',  #1232 ) ;
#3351=DIRECTION ( 'NONE',  ( 0.000000000000000000, 0.000000000000000000, -1.000000000000000000 ) ) ;
#3367=DIRECTION ( 'NONE',  ( 0.000000000000000000, 0.000000000000000000, -1.000000000000000000 ) ) ;
#3378=CIRCLE ( 'NONE', #3444, 7.000000000000000000 ) ;
#3390=DIRECTION ( 'NONE',  ( -1.000000000000000000, -0.000000000000000000, -0.000000000000000000 ) ) ;
#3411=EDGE_LOOP ( 'NONE', ( #1854, #3110, #3055, #1293 ) ) ;
#3421=DIRECTION ( 'NONE',  ( 1.000000000000000000, 0.000000000000000000, 0.000000000000000000 ) ) ;
#3444=AXIS2_PLACEMENT_3D ( 'NONE', #2831, #713, #163 ) ;
#3450=ADVANCED_FACE ( 'NONE', ( #2290, #2107 ), #3291, .F. ) ;
#3485=ORIENTED_EDGE ( 'NONE', *, *, #2050, .T. ) ;
#3499=CIRCLE ( 'NONE', #1822, 7.000000000000000000 ) ;
#3509=UNCERTAINTY_MEASURE_WITH_UNIT (LENGTH_MEASURE( 1.000000000000000082E-05 ), #3759, 'distance_accuracy_value', 'NONE');
#3511=LINE ( 'NONE', #811, #2874 ) ;
#3537=DIRECTION ( 'NONE',  ( 1.000000000000000000, 0.000000000000000000, 0.000000000000000000 ) ) ;
#3612=PRODUCT ( 'plain washer 10669 type nl_iso_ISO 10669-5.4-N', 'plain washer 10669 type nl_iso_ISO 10669-5.4-N', '', ( #1659 ) ) ;
#3627=DIRECTION ( 'NONE',  ( 1.000000000000000000, 0.000000000000000000, 0.000000000000000000 ) ) ;
#3628=EDGE_LOOP ( 'NONE', ( #1941, #601 ) ) ;
#3657=FILL_AREA_STYLE_COLOUR ( '', #2145 ) ;
#3658=EDGE_CURVE ( 'NONE', #208, #1281, #2327, .T. ) ;
#3669=DIRECTION ( 'NONE',  ( 0.000000000000000000, 0.000000000000000000, -1.000000000000000000 ) ) ;
#3688=CYLINDRICAL_SURFACE ( 'NONE', #3078, 7.000000000000000000 ) ;
#3693=EDGE_CURVE ( 'NONE', #2736, #201, #3499, .T. ) ;
#3707=ORIENTED_EDGE ( 'NONE', *, *, #2283, .T. ) ;
#3716=DIRECTION ( 'NONE',  ( 0.000000000000000000, 0.000000000000000000, 1.000000000000000000 ) ) ;
#3752=VERTEX_POINT ( 'NONE', #2180 ) ;
#3759=( LENGTH_UNIT ( ) NAMED_UNIT ( * ) SI_UNIT ( .MILLI., .METRE. ) );
#3791=LINE ( 'NONE', #2334, #2695 ) ;
#3875=COLOUR_RGB('Black',0.12,0.14,0.17);
#3876=FILL_AREA_STYLE_COLOUR('',#3875);
#3877=FILL_AREA_STYLE('',(#3876));
#3878=SURFACE_STYLE_FILL_AREA(#3877);
#3879=SURFACE_SIDE_STYLE('',(#3878));
#3880=SURFACE_STYLE_USAGE(.BOTH.,#3879);
#3881=PRESENTATION_STYLE_ASSIGNMENT((#3880));
ENDSEC;
END-ISO-10303-21;
